ISO-10303-21;
HEADER;
FILE_DESCRIPTION (('STEP AP214'),
    '1' );
FILE_NAME ('Pin 2X4.step',
    '2026-10-22T18:53:08',
    ( '' ),
    ( '' ),
    'SwSTEP 2.0',
    'SolidWorks 2025',
    '' );
FILE_SCHEMA (( 'AUTOMOTIVE_DESIGN' ));
ENDSEC;

DATA;
#86=DIRECTION ( 'NONE',  ( 1.000000000000000000, 0.000000000000000000, 0.000000000000000000 ) ) ;
#294=EDGE_CURVE ( 'NONE', #21978, #15166, #2770, .T. ) ;
#313=CIRCLE ( 'NONE', #1505, 1.000000000000000222 ) ;
#473=CONICAL_SURFACE ( 'NONE', #21125, 1.000000000000000222, 0.7853981633974508325 ) ;
#653=AXIS2_PLACEMENT_3D ( 'NONE', #18782, #3905, #4166 ) ;
#805=DIRECTION ( 'NONE',  ( -0.000000000000000000, -0.000000000000000000, -1.000000000000000000 ) ) ;
#809=AXIS2_PLACEMENT_3D ( 'NONE', #22982, #8323, #7950 ) ;
#849=SHAPE_REPRESENTATION_RELATIONSHIP ( 'NONE' , 'NONE' ,  #7043, #16009 ) ;
#955=LINE ( 'NONE', #8125, #3358 ) ;
#1098=DIRECTION ( 'NONE',  ( -0.000000000000000000, -0.000000000000000000, -1.000000000000000000 ) ) ;
#1143=ORIENTED_EDGE ( 'NONE', *, *, #13907, .T. ) ;
#1205=ADVANCED_FACE ( 'NONE', ( #12532 ), #8625, .T. ) ;
#1217=ORIENTED_EDGE ( 'NONE', *, *, #4231, .T. ) ;
#1421=EDGE_LOOP ( 'NONE', ( #21332, #19212, #5231, #17861 ) ) ;
#1432=VECTOR ( 'NONE', #18179, 1000.000000000000114 ) ;
#1505=AXIS2_PLACEMENT_3D ( 'NONE', #16896, #1795, #86 ) ;
#1604=EDGE_CURVE ( 'NONE', #12835, #16165, #10960, .T. ) ;
#1606=CARTESIAN_POINT ( 'NONE',  ( 0.000000000000000000, 0.000000000000000000, 0.2999999999999990452 ) ) ;
#1625=DIRECTION ( 'NONE',  ( -0.000000000000000000, -0.000000000000000000, -1.000000000000000000 ) ) ;
#1708=CARTESIAN_POINT ( 'NONE',  ( 0.000000000000000000, 0.000000000000000000, 4.000000000000000000 ) ) ;
#1795=DIRECTION ( 'NONE',  ( 0.000000000000000000, 0.000000000000000000, -1.000000000000000000 ) ) ;
#2770=LINE ( 'NONE', #6303, #14744 ) ;
#2912=ADVANCED_FACE ( 'NONE', ( #18190 ), #3645, .F. ) ;
#2993=AXIS2_PLACEMENT_3D ( 'NONE', #14742, #9129, #16575 ) ;
#3054=DIRECTION ( 'NONE',  ( -1.000000000000000000, 0.000000000000000000, 0.000000000000000000 ) ) ;
#3062=LINE ( 'NONE', #6957, #3598 ) ;
#3094=DIRECTION ( 'NONE',  ( -1.000000000000000000, 0.000000000000000000, 0.000000000000000000 ) ) ;
#3101=EDGE_LOOP ( 'NONE', ( #17105, #17595, #1143, #7292 ) ) ;
#3321=EDGE_CURVE ( 'NONE', #16165, #12835, #313, .T. ) ;
#3358=VECTOR ( 'NONE', #17650, 1000.000000000000000 ) ;
#3598=VECTOR ( 'NONE', #17828, 1000.000000000000114 ) ;
#3645=PLANE ( 'NONE',  #2993 ) ;
#3721=DIRECTION ( 'NONE',  ( 0.7071067811865457964, 8.659560562354910671E-17, -0.7071067811865492381 ) ) ;
#3747=VECTOR ( 'NONE', #1625, 1000.000000000000000 ) ;
#3750=VERTEX_POINT ( 'NONE', #6284 ) ;
#3816=ADVANCED_FACE ( 'NONE', ( #13866 ), #13609, .T. ) ;
#3905=DIRECTION ( 'NONE',  ( 0.000000000000000000, 0.000000000000000000, 1.000000000000000000 ) ) ;
#3988=( NAMED_UNIT ( * ) SI_UNIT ( $, .STERADIAN. ) SOLID_ANGLE_UNIT ( ) );
#4166=DIRECTION ( 'NONE',  ( 1.000000000000000000, 0.000000000000000000, 0.000000000000000000 ) ) ;
#4231=EDGE_CURVE ( 'NONE', #15166, #5560, #11284, .T. ) ;
#4673=AXIS2_PLACEMENT_3D ( 'NONE', #8100, #805, #19363 ) ;
#4947=ORIENTED_EDGE ( 'NONE', *, *, #22126, .T. ) ;
#5078=ADVANCED_FACE ( 'NONE', ( #14506 ), #21743, .T. ) ;
#5197=AXIS2_PLACEMENT_3D ( 'NONE', #9984, #20992, #6220 ) ;
#5231=ORIENTED_EDGE ( 'NONE', *, *, #294, .T. ) ;
#5255=VECTOR ( 'NONE', #3721, 1000.000000000000114 ) ;
#5367=EDGE_CURVE ( 'NONE', #3750, #12835, #7825, .T. ) ;
#5436=ORIENTED_EDGE ( 'NONE', *, *, #15696, .F. ) ;
#5560=VERTEX_POINT ( 'NONE', #8331 ) ;
#5703=PRODUCT ( 'Pin 2X4', 'Pin 2X4', '', ( #18854 ) ) ;
#5747=ADVANCED_FACE ( 'NONE', ( #19823 ), #15311, .T. ) ;
#5804=ORIENTED_EDGE ( 'NONE', *, *, #5367, .T. ) ;
#5941=( LENGTH_UNIT ( ) NAMED_UNIT ( * ) SI_UNIT ( .MILLI., .METRE. ) );
#5978=CARTESIAN_POINT ( 'NONE',  ( 0.000000000000000000, 0.000000000000000000, 0.000000000000000000 ) ) ;
#6029=CARTESIAN_POINT ( 'NONE',  ( 0.7000000000000005107, 8.572527594031479353E-17, 4.000000000000000000 ) ) ;
#6073=VERTEX_POINT ( 'NONE', #6257 ) ;
#6220=DIRECTION ( 'NONE',  ( 1.000000000000000000, 0.000000000000000000, 0.000000000000000000 ) ) ;
#6257=CARTESIAN_POINT ( 'NONE',  ( -0.6999999999999996225, 1.040949779275250140E-16, 0.000000000000000000 ) ) ;
#6284=CARTESIAN_POINT ( 'NONE',  ( 0.7000000000000005107, 1.040949779275250633E-16, 4.000000000000000000 ) ) ;
#6303=CARTESIAN_POINT ( 'NONE',  ( 1.000000000000000222, 0.000000000000000000, 0.2999999999999990452 ) ) ;
#6323=CARTESIAN_POINT ( 'NONE',  ( 0.000000000000000000, 0.000000000000000000, 0.000000000000000000 ) ) ;
#6345=DIRECTION ( 'NONE',  ( 1.000000000000000000, 0.000000000000000000, 0.000000000000000000 ) ) ;
#6360=AXIS2_PLACEMENT_3D ( 'NONE', #6323, #1098, #11795 ) ;
#6740=CONICAL_SURFACE ( 'NONE', #21943, 1.000000000000000222, 0.7853981633974508325 ) ;
#6892=CIRCLE ( 'NONE', #653, 0.7000000000000005107 ) ;
#6957=CARTESIAN_POINT ( 'NONE',  ( -1.000000000000000222, 1.224646799147353454E-16, 0.2999999999999990452 ) ) ;
#7043=SHAPE_REPRESENTATION ( 'Pin 2X4', ( #8005 ), #19339 ) ;
#7292=ORIENTED_EDGE ( 'NONE', *, *, #1604, .F. ) ;
#7509=CIRCLE ( 'NONE', #5197, 0.6999999999999996225 ) ;
#7517=CARTESIAN_POINT ( 'NONE',  ( 0.6999999999999996225, 0.000000000000000000, 0.000000000000000000 ) ) ;
#7825=LINE ( 'NONE', #6029, #5255 ) ;
#7950=DIRECTION ( 'NONE',  ( 1.000000000000000000, 0.000000000000000000, 0.000000000000000000 ) ) ;
#8005=AXIS2_PLACEMENT_3D ( 'NONE', #5978, #22344, #13412 ) ;
#8007=ORIENTED_EDGE ( 'NONE', *, *, #14039, .T. ) ;
#8100=CARTESIAN_POINT ( 'NONE',  ( 0.000000000000000000, 0.000000000000000000, 4.000000000000000000 ) ) ;
#8125=CARTESIAN_POINT ( 'NONE',  ( -1.000000000000000222, 0.000000000000000000, 4.000000000000000000 ) ) ;
#8241=PRODUCT_DEFINITION ( 'UNKNOWN', '', #18571, #13589 ) ;
#8270=( LENGTH_UNIT ( ) NAMED_UNIT ( * ) SI_UNIT ( .MILLI., .METRE. ) );
#8323=DIRECTION ( 'NONE',  ( -0.000000000000000000, -0.000000000000000000, 1.000000000000000000 ) ) ;
#8331=CARTESIAN_POINT ( 'NONE',  ( -1.000000000000000222, 0.000000000000000000, 0.2999999999999990452 ) ) ;
#8368=CIRCLE ( 'NONE', #9519, 1.000000000000000222 ) ;
#8474=EDGE_CURVE ( 'NONE', #21978, #6073, #22672, .T. ) ;
#8608=ORIENTED_EDGE ( 'NONE', *, *, #294, .F. ) ;
#8625=CONICAL_SURFACE ( 'NONE', #15281, 0.7000000000000005107, 0.7853981633974458365 ) ;
#8632=ORIENTED_EDGE ( 'NONE', *, *, #18850, .F. ) ;
#8765=ORIENTED_EDGE ( 'NONE', *, *, #15696, .T. ) ;
#8858=ORIENTED_EDGE ( 'NONE', *, *, #13630, .T. ) ;
#9025=AXIS2_PLACEMENT_3D ( 'NONE', #22580, #13666, #13427 ) ;
#9129=DIRECTION ( 'NONE',  ( 0.000000000000000000, 0.000000000000000000, 1.000000000000000000 ) ) ;
#9519=AXIS2_PLACEMENT_3D ( 'NONE', #14114, #12023, #23294 ) ;
#9652=ORIENTED_EDGE ( 'NONE', *, *, #22126, .F. ) ;
#9984=CARTESIAN_POINT ( 'NONE',  ( 0.000000000000000000, 0.000000000000000000, 0.000000000000000000 ) ) ;
#10328=DIRECTION ( 'NONE',  ( 0.7071067811865492381, 0.000000000000000000, 0.7071067811865457964 ) ) ;
#10332=CARTESIAN_POINT ( 'NONE',  ( -1.000000000000000222, 0.000000000000000000, 3.699999999999998845 ) ) ;
#10521=ADVANCED_FACE ( 'NONE', ( #21817 ), #16072, .T. ) ;
#10707=LINE ( 'NONE', #12661, #1432 ) ;
#10748=EDGE_LOOP ( 'NONE', ( #19567, #8858, #1217, #9652 ) ) ;
#10960=CIRCLE ( 'NONE', #9025, 1.000000000000000222 ) ;
#11147=CARTESIAN_POINT ( 'NONE',  ( 1.000000000000000222, 1.224646799147353454E-16, 0.2999999999999990452 ) ) ;
#11284=CIRCLE ( 'NONE', #809, 1.000000000000000222 ) ;
#11348=AXIS2_PLACEMENT_3D ( 'NONE', #14127, #12296, #14245 ) ;
#11407=ADVANCED_FACE ( 'NONE', ( #15597 ), #473, .T. ) ;
#11529=ORIENTED_EDGE ( 'NONE', *, *, #4231, .F. ) ;
#11549=UNCERTAINTY_MEASURE_WITH_UNIT (LENGTH_MEASURE( 1.000000000000000082E-05 ), #5941, 'distance_accuracy_value', 'NONE');
#11631=EDGE_CURVE ( 'NONE', #6073, #5560, #3062, .T. ) ;
#11795=DIRECTION ( 'NONE',  ( 1.000000000000000000, 0.000000000000000000, 0.000000000000000000 ) ) ;
#12023=DIRECTION ( 'NONE',  ( -0.000000000000000000, -0.000000000000000000, 1.000000000000000000 ) ) ;
#12296=DIRECTION ( 'NONE',  ( 0.000000000000000000, 0.000000000000000000, 1.000000000000000000 ) ) ;
#12432=DIRECTION ( 'NONE',  ( 0.000000000000000000, 0.000000000000000000, 1.000000000000000000 ) ) ;
#12456=FACE_OUTER_BOUND ( 'NONE', #20807, .T. ) ;
#12532=FACE_OUTER_BOUND ( 'NONE', #13810, .T. ) ;
#12661=CARTESIAN_POINT ( 'NONE',  ( -0.7000000000000005107, 0.000000000000000000, 4.000000000000000000 ) ) ;
#12741=APPLICATION_CONTEXT ( 'automotive_design' ) ;
#12835=VERTEX_POINT ( 'NONE', #20896 ) ;
#13036=AXIS2_PLACEMENT_3D ( 'NONE', #23578, #23802, #21976 ) ;
#13412=DIRECTION ( 'NONE',  ( 1.000000000000000000, 0.000000000000000000, 0.000000000000000000 ) ) ;
#13427=DIRECTION ( 'NONE',  ( 1.000000000000000000, 0.000000000000000000, 0.000000000000000000 ) ) ;
#13589=PRODUCT_DEFINITION_CONTEXT ( 'detailed design', #14630, 'design' ) ;
#13609=CYLINDRICAL_SURFACE ( 'NONE', #4673, 1.000000000000000222 ) ;
#13630=EDGE_CURVE ( 'NONE', #12835, #15166, #14547, .T. ) ;
#13665=STYLED_ITEM('',(#24155),#18330);
#13666=DIRECTION ( 'NONE',  ( 0.000000000000000000, 0.000000000000000000, -1.000000000000000000 ) ) ;
#13781=( NAMED_UNIT ( * ) SI_UNIT ( $, .STERADIAN. ) SOLID_ANGLE_UNIT ( ) );
#13792=DIRECTION ( 'NONE',  ( -0.000000000000000000, -0.000000000000000000, 1.000000000000000000 ) ) ;
#13810=EDGE_LOOP ( 'NONE', ( #8632, #5804, #21440, #24003 ) ) ;
#13866=FACE_OUTER_BOUND ( 'NONE', #18561, .T. ) ;
#13907=EDGE_CURVE ( 'NONE', #17649, #16165, #10707, .T. ) ;
#14039=EDGE_CURVE ( 'NONE', #17649, #3750, #6892, .T. ) ;
#14112=ORIENTED_EDGE ( 'NONE', *, *, #1604, .T. ) ;
#14114=CARTESIAN_POINT ( 'NONE',  ( 0.000000000000000000, 0.000000000000000000, 0.2999999999999990452 ) ) ;
#14127=CARTESIAN_POINT ( 'NONE',  ( 0.000000000000000000, 0.000000000000000000, 4.000000000000000000 ) ) ;
#14245=DIRECTION ( 'NONE',  ( 1.000000000000000000, 0.000000000000000000, -0.000000000000000000 ) ) ;
#14355=CLOSED_SHELL ( 'NONE', ( #1205, #15482, #5078, #3816, #10521, #2912, #11407, #5747 ) ) ;
#14415=CARTESIAN_POINT ( 'NONE',  ( 0.000000000000000000, 0.000000000000000000, 4.000000000000000000 ) ) ;
#14464=ORIENTED_EDGE ( 'NONE', *, *, #15026, .T. ) ;
#14506=FACE_OUTER_BOUND ( 'NONE', #10748, .T. ) ;
#14547=LINE ( 'NONE', #16370, #3747 ) ;
#14630=APPLICATION_CONTEXT ( 'automotive_design' ) ;
#14742=CARTESIAN_POINT ( 'NONE',  ( 0.000000000000000000, 0.000000000000000000, 0.000000000000000000 ) ) ;
#14744=VECTOR ( 'NONE', #10328, 1000.000000000000114 ) ;
#14956=( NAMED_UNIT ( * ) PLANE_ANGLE_UNIT ( ) SI_UNIT ( $, .RADIAN. ) );
#15026=EDGE_CURVE ( 'NONE', #5560, #15166, #8368, .T. ) ;
#15044=EDGE_LOOP ( 'NONE', ( #24005, #8765 ) ) ;
#15166=VERTEX_POINT ( 'NONE', #11147 ) ;
#15189=EDGE_LOOP ( 'NONE', ( #8007, #16560 ) ) ;
#15281=AXIS2_PLACEMENT_3D ( 'NONE', #21722, #16326, #3054 ) ;
#15311=CONICAL_SURFACE ( 'NONE', #22735, 0.7000000000000005107, 0.7853981633974458365 ) ;
#15360=CARTESIAN_POINT ( 'NONE',  ( 0.000000000000000000, 0.000000000000000000, 0.2999999999999990452 ) ) ;
#15482=ADVANCED_FACE ( 'NONE', ( #12456 ), #6740, .T. ) ;
#15499=ORIENTED_EDGE ( 'NONE', *, *, #11631, .T. ) ;
#15597=FACE_OUTER_BOUND ( 'NONE', #1421, .T. ) ;
#15696=EDGE_CURVE ( 'NONE', #6073, #21978, #7509, .T. ) ;
#15909=CARTESIAN_POINT ( 'NONE',  ( -0.7000000000000005107, 0.000000000000000000, 4.000000000000000000 ) ) ;
#16009=ADVANCED_BREP_SHAPE_REPRESENTATION ( '', ( #18330, #8005 ), #19339 ) ;
#16072=PLANE ( 'NONE',  #11348 ) ;
#16165=VERTEX_POINT ( 'NONE', #10332 ) ;
#16326=DIRECTION ( 'NONE',  ( 0.000000000000000000, 0.000000000000000000, -1.000000000000000000 ) ) ;
#16370=CARTESIAN_POINT ( 'NONE',  ( 1.000000000000000222, 1.224646799147353454E-16, 4.000000000000000000 ) ) ;
#16560=ORIENTED_EDGE ( 'NONE', *, *, #18850, .T. ) ;
#16575=DIRECTION ( 'NONE',  ( 1.000000000000000000, 0.000000000000000000, -0.000000000000000000 ) ) ;
#16757=SHAPE_DEFINITION_REPRESENTATION ( #21913, #7043 ) ;
#16896=CARTESIAN_POINT ( 'NONE',  ( 0.000000000000000000, 0.000000000000000000, 3.699999999999998845 ) ) ;
#17105=ORIENTED_EDGE ( 'NONE', *, *, #5367, .F. ) ;
#17595=ORIENTED_EDGE ( 'NONE', *, *, #14039, .F. ) ;
#17649=VERTEX_POINT ( 'NONE', #15909 ) ;
#17650=DIRECTION ( 'NONE',  ( -0.000000000000000000, -0.000000000000000000, -1.000000000000000000 ) ) ;
#17828=DIRECTION ( 'NONE',  ( -0.7071067811865492381, 8.659560562354955045E-17, 0.7071067811865457964 ) ) ;
#17861=ORIENTED_EDGE ( 'NONE', *, *, #15026, .F. ) ;
#17963=MECHANICAL_DESIGN_GEOMETRIC_PRESENTATION_REPRESENTATION('',(#13665),#22248);
#18091=DIRECTION ( 'NONE',  ( -0.000000000000000000, -0.000000000000000000, 1.000000000000000000 ) ) ;
#18179=DIRECTION ( 'NONE',  ( -0.7071067811865457964, 0.000000000000000000, -0.7071067811865492381 ) ) ;
#18190=FACE_OUTER_BOUND ( 'NONE', #15044, .T. ) ;
#18330=MANIFOLD_SOLID_BREP ( 'Chamfer1', #14355 ) ;
#18561=EDGE_LOOP ( 'NONE', ( #23200, #14112, #4947, #14464 ) ) ;
#18571=PRODUCT_DEFINITION_FORMATION_WITH_SPECIFIED_SOURCE ( 'ANY', '', #5703, .NOT_KNOWN. ) ;
#18782=CARTESIAN_POINT ( 'NONE',  ( 0.000000000000000000, 0.000000000000000000, 4.000000000000000000 ) ) ;
#18850=EDGE_CURVE ( 'NONE', #3750, #17649, #21499, .T. ) ;
#18854=PRODUCT_CONTEXT ( 'NONE', #12741, 'mechanical' ) ;
#19212=ORIENTED_EDGE ( 'NONE', *, *, #8474, .F. ) ;
#19339=( GEOMETRIC_REPRESENTATION_CONTEXT ( 3 ) GLOBAL_UNCERTAINTY_ASSIGNED_CONTEXT ( ( #19626 ) ) GLOBAL_UNIT_ASSIGNED_CONTEXT ( ( #8270, #23319, #13781 ) ) REPRESENTATION_CONTEXT ( 'NONE', 'WORKASPACE' ) );
#19363=DIRECTION ( 'NONE',  ( -1.000000000000000000, 0.000000000000000000, 0.000000000000000000 ) ) ;
#19567=ORIENTED_EDGE ( 'NONE', *, *, #3321, .T. ) ;
#19626=UNCERTAINTY_MEASURE_WITH_UNIT (LENGTH_MEASURE( 1.000000000000000082E-05 ), #8270, 'distance_accuracy_value', 'NONE');
#19823=FACE_OUTER_BOUND ( 'NONE', #3101, .T. ) ;
#20807=EDGE_LOOP ( 'NONE', ( #5436, #15499, #11529, #8608 ) ) ;
#20896=CARTESIAN_POINT ( 'NONE',  ( 1.000000000000000222, 1.224646799147353454E-16, 3.699999999999998845 ) ) ;
#20992=DIRECTION ( 'NONE',  ( -0.000000000000000000, -0.000000000000000000, -1.000000000000000000 ) ) ;
#21125=AXIS2_PLACEMENT_3D ( 'NONE', #15360, #13792, #6345 ) ;
#21332=ORIENTED_EDGE ( 'NONE', *, *, #11631, .F. ) ;
#21440=ORIENTED_EDGE ( 'NONE', *, *, #3321, .F. ) ;
#21499=CIRCLE ( 'NONE', #22259, 0.7000000000000005107 ) ;
#21722=CARTESIAN_POINT ( 'NONE',  ( 0.000000000000000000, 0.000000000000000000, 4.000000000000000000 ) ) ;
#21743=CYLINDRICAL_SURFACE ( 'NONE', #13036, 1.000000000000000222 ) ;
#21817=FACE_OUTER_BOUND ( 'NONE', #15189, .T. ) ;
#21913=PRODUCT_DEFINITION_SHAPE ( 'NONE', 'NONE',  #8241 ) ;
#21943=AXIS2_PLACEMENT_3D ( 'NONE', #1606, #18091, #23707 ) ;
#21976=DIRECTION ( 'NONE',  ( -1.000000000000000000, 0.000000000000000000, 0.000000000000000000 ) ) ;
#21978=VERTEX_POINT ( 'NONE', #7517 ) ;
#22126=EDGE_CURVE ( 'NONE', #16165, #5560, #955, .T. ) ;
#22248=( GEOMETRIC_REPRESENTATION_CONTEXT ( 3 ) GLOBAL_UNCERTAINTY_ASSIGNED_CONTEXT ( ( #11549 ) ) GLOBAL_UNIT_ASSIGNED_CONTEXT ( ( #5941, #14956, #3988 ) ) REPRESENTATION_CONTEXT ( 'NONE', 'WORKASPACE' ) );
#22259=AXIS2_PLACEMENT_3D ( 'NONE', #1708, #12432, #23914 ) ;
#22344=DIRECTION ( 'NONE',  ( 0.000000000000000000, 0.000000000000000000, 1.000000000000000000 ) ) ;
#22580=CARTESIAN_POINT ( 'NONE',  ( 0.000000000000000000, 0.000000000000000000, 3.699999999999998845 ) ) ;
#22672=CIRCLE ( 'NONE', #6360, 0.6999999999999996225 ) ;
#22735=AXIS2_PLACEMENT_3D ( 'NONE', #14415, #23822, #3094 ) ;
#22982=CARTESIAN_POINT ( 'NONE',  ( 0.000000000000000000, 0.000000000000000000, 0.2999999999999990452 ) ) ;
#23200=ORIENTED_EDGE ( 'NONE', *, *, #13630, .F. ) ;
#23294=DIRECTION ( 'NONE',  ( 1.000000000000000000, 0.000000000000000000, 0.000000000000000000 ) ) ;
#23319=( NAMED_UNIT ( * ) PLANE_ANGLE_UNIT ( ) SI_UNIT ( $, .RADIAN. ) );
#23578=CARTESIAN_POINT ( 'NONE',  ( 0.000000000000000000, 0.000000000000000000, 4.000000000000000000 ) ) ;
#23707=DIRECTION ( 'NONE',  ( 1.000000000000000000, 0.000000000000000000, 0.000000000000000000 ) ) ;
#23802=DIRECTION ( 'NONE',  ( -0.000000000000000000, -0.000000000000000000, -1.000000000000000000 ) ) ;
#23822=DIRECTION ( 'NONE',  ( 0.000000000000000000, 0.000000000000000000, -1.000000000000000000 ) ) ;
#23914=DIRECTION ( 'NONE',  ( 1.000000000000000000, 0.000000000000000000, 0.000000000000000000 ) ) ;
#24003=ORIENTED_EDGE ( 'NONE', *, *, #13907, .F. ) ;
#24005=ORIENTED_EDGE ( 'NONE', *, *, #8474, .T. ) ;
#24149=COLOUR_RGB('Grey',0.48,0.52,0.57);
#24150=FILL_AREA_STYLE_COLOUR('',#24149);
#24151=FILL_AREA_STYLE('',(#24150));
#24152=SURFACE_STYLE_FILL_AREA(#24151);
#24153=SURFACE_SIDE_STYLE('',(#24152));
#24154=SURFACE_STYLE_USAGE(.BOTH.,#24153);
#24155=PRESENTATION_STYLE_ASSIGNMENT((#24154));
ENDSEC;
END-ISO-10303-21;
